ISO-10303-21;
HEADER;
FILE_DESCRIPTION (('STEP AP203'),
    '1' );
FILE_NAME ('1602p_c_45.step',
    '2026-10-31T14:11:27',
    ( '' ),
    ( '' ),
    'SwSTEP 2.0',
    'SolidWorks 2024',
    '' );
FILE_SCHEMA (( 'AUTOMOTIVE_DESIGN' ));
ENDSEC;

DATA;
#67=EDGE_CURVE ( 'NONE', #14097, #1408, #5016, .T. ) ;
#100=DIRECTION ( 'NONE',  ( 0.1153179901961009640, 0.4865200521429018377, 0.8660254037844385966 ) ) ;
#137=CARTESIAN_POINT ( 'NONE',  ( 31.37708959083939675, -0.2124270449897310287, 13.00000000000019895 ) ) ;
#150=ORIENTED_EDGE ( 'NONE', *, *, #9051, .F. ) ;
#169=DIRECTION ( 'NONE',  ( -9.594916218540590128E-33, 2.583840697242805182E-16, -1.000000000000000000 ) ) ;
#182=AXIS2_PLACEMENT_3D ( 'NONE', #3666, #10943, #21940 ) ;
#215=EDGE_CURVE ( 'NONE', #11840, #10096, #7770, .T. ) ;
#220=CARTESIAN_POINT ( 'NONE',  ( 29.36184298829670070, -3.294841866349740300, 15.00000000000000000 ) ) ;
#271=FACE_OUTER_BOUND ( 'NONE', #1548, .T. ) ;
#306=VERTEX_POINT ( 'NONE', #5482 ) ;
#327=ORIENTED_EDGE ( 'NONE', *, *, #22096, .F. ) ;
#388=CARTESIAN_POINT ( 'NONE',  ( 28.14554285793940025, -3.006546890859489896, 15.00000000000000000 ) ) ;
#415=DIRECTION ( 'NONE',  ( 1.000000000000000000, 0.000000000000000000, 0.000000000000000000 ) ) ;
#419=CARTESIAN_POINT ( 'NONE',  ( 30.89467803343008967, -3.022216679643965342, 15.00000000000011724 ) ) ;
#439=CARTESIAN_POINT ( 'NONE',  ( 43.98050001724080005, -5.573152644851309567, 15.50000000000019895 ) ) ;
#451=AXIS2_PLACEMENT_3D ( 'NONE', #12252, #19482, #8439 ) ;
#494=CARTESIAN_POINT ( 'NONE',  ( 52.49909637502329929, -7.592283011512489743, 15.25462000000019991 ) ) ;
#550=CARTESIAN_POINT ( 'NONE',  ( 33.37436288052550282, -3.059220458576299873, 13.00000000000019895 ) ) ;
#565=DIRECTION ( 'NONE',  ( 0.9730401042858036753, -0.2306359803922028995, -5.432877459303547669E-17 ) ) ;
#584=EDGE_LOOP ( 'NONE', ( #9967, #15754, #19840, #6241, #22801 ) ) ;
#612=ORIENTED_EDGE ( 'NONE', *, *, #6730, .F. ) ;
#622=CARTESIAN_POINT ( 'NONE',  ( 52.49909637502329929, -7.592283011512489743, 13.00000000000019895 ) ) ;
#648=VECTOR ( 'NONE', #22926, 999.9999999999998863 ) ;
#663=DIRECTION ( 'NONE',  ( 0.9730401042858035643, -0.2306359803922028717, -5.432877459303547053E-17 ) ) ;
#871=DIRECTION ( 'NONE',  ( -0.6880432561069586006, 0.1630842657209347069, -0.7071067811865459074 ) ) ;
#893=AXIS2_PLACEMENT_3D ( 'NONE', #20849, #2461, #4233 ) ;
#908=DIRECTION ( 'NONE',  ( -0.9730401042858035643, 0.2306359803922028717, 5.432877459303547053E-17 ) ) ;
#923=ORIENTED_EDGE ( 'NONE', *, *, #4260, .T. ) ;
#1146=( GEOMETRIC_REPRESENTATION_CONTEXT ( 3 ) GLOBAL_UNCERTAINTY_ASSIGNED_CONTEXT ( ( #22398 ) ) GLOBAL_UNIT_ASSIGNED_CONTEXT ( ( #19948, #21719, #9375 ) ) REPRESENTATION_CONTEXT ( 'NONE', 'WORKASPACE' ) );
#1205=CARTESIAN_POINT ( 'NONE',  ( 52.73786095581300515, -7.648876468381129889, 11.75000000000019895 ) ) ;
#1210=CARTESIAN_POINT ( 'NONE',  ( 33.27705887009690144, -3.036156860537079893, 13.00000000000019895 ) ) ;
#1242=PLANE ( 'NONE',  #5424 ) ;
#1274=CIRCLE ( 'NONE', #3919, 4.250000000000000000 ) ;
#1276=AXIS2_PLACEMENT_3D ( 'NONE', #4483, #18628, #4128 ) ;
#1294=ORIENTED_EDGE ( 'NONE', *, *, #1980, .T. ) ;
#1320=ORIENTED_EDGE ( 'NONE', *, *, #19192, .T. ) ;
#1391=CIRCLE ( 'NONE', #19983, 4.250000000000000000 ) ;
#1408=VERTEX_POINT ( 'NONE', #6093 ) ;
#1444=AXIS2_PLACEMENT_3D ( 'NONE', #17981, #1562, #3353 ) ;
#1463=CARTESIAN_POINT ( 'NONE',  ( 31.49315201223960159, -2.613324229818040134, 14.15470053837944953 ) ) ;
#1499=TOROIDAL_SURFACE ( 'NONE', #8729, 3.750000000000000000, 0.5000000000000000000 ) ;
#1548=EDGE_LOOP ( 'NONE', ( #18129, #6141, #23227, #20317, #3227 ) ) ;
#1551=CARTESIAN_POINT ( 'NONE',  ( 30.57814311865390167, -3.583136841839989817, 11.00000000000019895 ) ) ;
#1562=DIRECTION ( 'NONE',  ( 0.9730401042858035643, -0.2306359803922028717, -5.432877459303547053E-17 ) ) ;
#1569=CARTESIAN_POINT ( 'NONE',  ( 31.56827854690379098, -0.8510906712621758574, 14.00000000000018296 ) ) ;
#1578=DIRECTION ( 'NONE',  ( 0.000000000000000000, 1.156482317317871478E-16, 1.000000000000000000 ) ) ;
#1604=DIRECTION ( 'NONE',  ( 0.000000000000000000, 0.000000000000000000, -1.000000000000000000 ) ) ;
#1607=DIRECTION ( 'NONE',  ( 0.1997366180463769070, 0.8426774492125652660, 0.5000000000000003331 ) ) ;
#1643=CONICAL_SURFACE ( 'NONE', #10786, 1.154700538379250796, 1.047197551196598297 ) ;
#1654=DIRECTION ( 'NONE',  ( 0.9730401042858035643, -0.2306359803922028717, -5.432877459303547053E-17 ) ) ;
#1673=DIRECTION ( 'NONE',  ( 0.000000000000000000, 0.000000000000000000, 1.000000000000000000 ) ) ;
#1694=VERTEX_POINT ( 'NONE', #20212 ) ;
#1717=CARTESIAN_POINT ( 'NONE',  ( 33.37436288052550282, -3.059220458576299873, 13.00000000000019895 ) ) ;
#1774=ORIENTED_EDGE ( 'NONE', *, *, #14842, .F. ) ;
#1798=AXIS2_PLACEMENT_3D ( 'NONE', #388, #4201, #22355 ) ;
#1980=EDGE_CURVE ( 'NONE', #12251, #20636, #6307, .T. ) ;
#2073=CARTESIAN_POINT ( 'NONE',  ( 28.94448933012489888, 0.3641629059907759425, 13.00000000000019895 ) ) ;
#2124=EDGE_LOOP ( 'NONE', ( #14350, #6851, #3150, #21931 ) ) ;
#2211=CARTESIAN_POINT ( 'NONE',  ( 28.54501609403219931, -1.321191992434360030, 11.00000000000019895 ) ) ;
#2220=ORIENTED_EDGE ( 'NONE', *, *, #6488, .T. ) ;
#2224=FACE_OUTER_BOUND ( 'NONE', #2124, .T. ) ;
#2248=AXIS2_PLACEMENT_3D ( 'NONE', #5616, #21993, #12987 ) ;
#2461=DIRECTION ( 'NONE',  ( 5.798605125234323991E-17, -1.374421231021384554E-17, 1.000000000000000000 ) ) ;
#2509=SHAPE_REPRESENTATION ( '1602p_c_45', ( #12739 ), #1146 ) ;
#2569=CARTESIAN_POINT ( 'NONE',  ( 0.000000000000000000, 0.000000000000000000, 0.000000000000000000 ) ) ;
#2578=AXIS2_PLACEMENT_3D ( 'NONE', #1717, #12540, #18230 ) ;
#2615=ORIENTED_EDGE ( 'NONE', *, *, #11565, .T. ) ;
#2633=LINE ( 'NONE', #9889, #648 ) ;
#2686=CARTESIAN_POINT ( 'NONE',  ( 30.57814311865390167, -3.583136841839989817, 15.00000000000000000 ) ) ;
#2771=EDGE_LOOP ( 'NONE', ( #17377, #612, #19152, #6273, #8122 ) ) ;
#2817=FACE_OUTER_BOUND ( 'NONE', #2771, .T. ) ;
#2829=CARTESIAN_POINT ( 'NONE',  ( 30.31182762792540331, -4.706706774123410320, 13.00000000000019895 ) ) ;
#2872=EDGE_CURVE ( 'NONE', #14790, #20287, #4872, .T. ) ;
#2939=EDGE_LOOP ( 'NONE', ( #13738, #7255 ) ) ;
#3018=VERTEX_POINT ( 'NONE', #6521 ) ;
#3049=ORIENTED_EDGE ( 'NONE', *, *, #14612, .F. ) ;
#3089=TOROIDAL_SURFACE ( 'NONE', #14850, 2.600000000000000089, 0.1000000000000000056 ) ;
#3148=LINE ( 'NONE', #1463, #5415 ) ;
#3150=ORIENTED_EDGE ( 'NONE', *, *, #13119, .T. ) ;
#3207=CYLINDRICAL_SURFACE ( 'NONE', #9593, 4.250000000000000000 ) ;
#3227=ORIENTED_EDGE ( 'NONE', *, *, #14039, .F. ) ;
#3243=LINE ( 'NONE', #10509, #9359 ) ;
#3278=FACE_OUTER_BOUND ( 'NONE', #20136, .T. ) ;
#3316=CIRCLE ( 'NONE', #16568, 2.009239999999998805 ) ;
#3353=DIRECTION ( 'NONE',  ( 0.000000000000000000, 0.000000000000000000, -1.000000000000000000 ) ) ;
#3392=CARTESIAN_POINT ( 'NONE',  ( 28.74475271207850113, -0.4785145432217889905, 14.50000000000020073 ) ) ;
#3448=DIRECTION ( 'NONE',  ( -0.9730401042858035643, 0.2306359803922028717, 5.959266323858677443E-17 ) ) ;
#3461=CARTESIAN_POINT ( 'NONE',  ( 52.49909637502329929, -7.592283011512489743, 13.00000000000019895 ) ) ;
#3499=AXIS2_PLACEMENT_3D ( 'NONE', #3461, #10732, #1673 ) ;
#3529=AXIS2_PLACEMENT_3D ( 'NONE', #19488, #1654, #21137 ) ;
#3608=DIRECTION ( 'NONE',  ( -0.1153179901961009640, -0.4865200521429018377, -0.8660254037844385966 ) ) ;
#3619=ADVANCED_FACE ( 'NONE', ( #3278 ), #8386, .F. ) ;
#3657=CARTESIAN_POINT ( 'NONE',  ( 30.31182762792540331, -4.706706774123410320, 13.00000000000019895 ) ) ;
#3666=CARTESIAN_POINT ( 'NONE',  ( 33.37436288052550282, -3.059220458576299873, 13.00000000000019895 ) ) ;
#3717=DIRECTION ( 'NONE',  ( 0.000000000000000000, 1.020425574104004122E-16, 1.000000000000000000 ) ) ;
#3737=CARTESIAN_POINT ( 'NONE',  ( 29.09552749756820234, -4.418411798633160359, 13.00000000000019895 ) ) ;
#3812=( BOUNDED_CURVE ( )  B_SPLINE_CURVE ( 2, ( #22358, #9567, #13124 ),
 .UNSPECIFIED., .F., .F. ) 
 B_SPLINE_CURVE_WITH_KNOTS ( ( 3, 3 ),
 ( 0.1168436138077928593, 0.2336872276155859962 ),
 .UNSPECIFIED. ) 
 CURVE ( )  GEOMETRIC_REPRESENTATION_ITEM ( )  RATIONAL_B_SPLINE_CURVE ( ( 1.077350269189624843, 1.077350269189625065, 1.000000000000000000 ) ) 
 REPRESENTATION_ITEM ( '' )  );
#3814=CARTESIAN_POINT ( 'NONE',  ( 29.36184298829670070, -3.294841866349740300, 11.00000000000019895 ) ) ;
#3827=EDGE_LOOP ( 'NONE', ( #10553, #1774, #20650, #7900 ) ) ;
#3860=DIRECTION ( 'NONE',  ( 0.9730401042858035643, -0.2306359803922028717, -5.959266323858674978E-17 ) ) ;
#3864=CARTESIAN_POINT ( 'NONE',  ( 29.89447396975369742, -1.047702001782899961, 15.00000000000000000 ) ) ;
#3894=ORIENTED_EDGE ( 'NONE', *, *, #4260, .F. ) ;
#3919=AXIS2_PLACEMENT_3D ( 'NONE', #9445, #7658, #14903 ) ;
#3986=DIRECTION ( 'NONE',  ( -0.9730401042858036753, 0.2306359803922028995, 5.959266323858677443E-17 ) ) ;
#4001=EDGE_LOOP ( 'NONE', ( #16150, #4133, #21391, #19693, #11776 ) ) ;
#4025=LINE ( 'NONE', #5816, #14226 ) ;
#4034=DIRECTION ( 'NONE',  ( -0.9730401042858036753, 0.2306359803922028995, 5.959266323858677443E-17 ) ) ;
#4128=DIRECTION ( 'NONE',  ( 0.000000000000000000, 1.000000000000000000, 0.000000000000000000 ) ) ;
#4133=ORIENTED_EDGE ( 'NONE', *, *, #19138, .T. ) ;
#4180=CARTESIAN_POINT ( 'NONE',  ( 30.84445860938240003, -2.459566909556569758, 17.25000000000019895 ) ) ;
#4193=ORIENTED_EDGE ( 'NONE', *, *, #7973, .T. ) ;
#4201=DIRECTION ( 'NONE',  ( 1.040345436475888435E-32, 1.169424102322700040E-16, 1.000000000000000000 ) ) ;
#4211=CARTESIAN_POINT ( 'NONE',  ( 31.01827548281339020, -2.500766059351007708, 11.00000000000020428 ) ) ;
#4233=DIRECTION ( 'NONE',  ( 1.000000000000000000, 0.000000000000000000, 0.000000000000000000 ) ) ;
#4234=EDGE_LOOP ( 'NONE', ( #5357, #22758, #13263, #4953 ) ) ;
#4238=ORIENTED_EDGE ( 'NONE', *, *, #20669, .T. ) ;
#4260=EDGE_CURVE ( 'NONE', #12862, #10685, #22957, .T. ) ;
#4261=VECTOR ( 'NONE', #17550, 1000.000000000000114 ) ;
#4363=CARTESIAN_POINT ( 'NONE',  ( 27.91817548414393713, -6.133715391986834575, 13.00000000000019895 ) ) ;
#4472=VERTEX_POINT ( 'NONE', #11582 ) ;
#4483=CARTESIAN_POINT ( 'NONE',  ( 29.76326332728156032, 1.650605442299594827, 13.00000000000019895 ) ) ;
#4498=DIRECTION ( 'NONE',  ( 0.9730401042858035643, -0.2306359803922028717, -5.959266323858677443E-17 ) ) ;
#4524=CARTESIAN_POINT ( 'NONE',  ( 30.57814311865390167, -3.583136841839989817, 11.00000000000019895 ) ) ;
#4547=FACE_OUTER_BOUND ( 'NONE', #21661, .T. ) ;
#4585=EDGE_CURVE ( 'NONE', #7299, #18104, #11101, .T. ) ;
#4601=VERTEX_POINT ( 'NONE', #15925 ) ;
#4684=CARTESIAN_POINT ( 'NONE',  ( 33.97401642954523737, -0.5293161874332097394, 13.00000000000019895 ) ) ;
#4755=DIRECTION ( 'NONE',  ( -0.1997366180463770735, -0.8426774492125654881, -0.4999999999999997780 ) ) ;
#4800=CARTESIAN_POINT ( 'NONE',  ( 31.49315201223960159, -2.613324229818040134, 11.84529946162094838 ) ) ;
#4805=VERTEX_POINT ( 'NONE', #21845 ) ;
#4872=( BOUNDED_CURVE ( )  B_SPLINE_CURVE ( 2, ( #9178, #1569, #137 ),
 .UNSPECIFIED., .F., .F. ) 
 B_SPLINE_CURVE_WITH_KNOTS ( ( 3, 3 ),
 ( 0.000000000000000000, 0.2336872276155859962 ),
 .UNSPECIFIED. ) 
 CURVE ( )  GEOMETRIC_REPRESENTATION_ITEM ( )  RATIONAL_B_SPLINE_CURVE ( ( 1.000000000000000000, 1.154700538379259900, 1.000000000000000000 ) ) 
 REPRESENTATION_ITEM ( '' )  );
#4892=CARTESIAN_POINT ( 'NONE',  ( 33.27705887009690144, -3.036156860537079893, 13.00000000000019895 ) ) ;
#4950=DIRECTION ( 'NONE',  ( 0.9286452767786566032, 1.871119812896368998E-17, -0.3709689338970208472 ) ) ;
#4953=ORIENTED_EDGE ( 'NONE', *, *, #17226, .F. ) ;
#4979=ORIENTED_EDGE ( 'NONE', *, *, #7066, .T. ) ;
#5012=ORIENTED_EDGE ( 'NONE', *, *, #18439, .F. ) ;
#5016=LINE ( 'NONE', #19273, #14852 ) ;
#5085=VECTOR ( 'NONE', #12689, 999.9999999999998863 ) ;
#5190=CIRCLE ( 'NONE', #18472, 4.250000000000000000 ) ;
#5275=FACE_OUTER_BOUND ( 'NONE', #12103, .T. ) ;
#5357=ORIENTED_EDGE ( 'NONE', *, *, #19814, .F. ) ;
#5383=CARTESIAN_POINT ( 'NONE',  ( 27.94580623989299895, -3.849224340072050055, 13.50000000000019895 ) ) ;
#5415=VECTOR ( 'NONE', #8726, 1000.000000000000114 ) ;
#5424=AXIS2_PLACEMENT_3D ( 'NONE', #6839, #20844, #19308 ) ;
#5460=SHAPE_REPRESENTATION_RELATIONSHIP ( 'NONE' , 'NONE' ,  #2509, #7943 ) ;
#5480=ORIENTED_EDGE ( 'NONE', *, *, #17700, .F. ) ;
#5482=CARTESIAN_POINT ( 'NONE',  ( 30.31182762792540331, -4.706706774123410320, 13.00000000000019895 ) ) ;
#5514=DIRECTION ( 'NONE',  ( -0.9730401042858035643, 0.2306359803922028717, 5.667427308550587516E-17 ) ) ;
#5615=ORIENTED_EDGE ( 'NONE', *, *, #5872, .T. ) ;
#5616=CARTESIAN_POINT ( 'NONE',  ( 28.41185834866789861, -1.882976958576060067, 9.720299461620909298 ) ) ;
#5620=ORIENTED_EDGE ( 'NONE', *, *, #18439, .T. ) ;
#5638=ORIENTED_EDGE ( 'NONE', *, *, #215, .F. ) ;
#5731=CARTESIAN_POINT ( 'NONE',  ( 28.41185834866789861, -1.882976958576060067, 13.00000000000019895 ) ) ;
#5732=FACE_OUTER_BOUND ( 'NONE', #18895, .T. ) ;
#5771=( BOUNDED_CURVE ( )  B_SPLINE_CURVE ( 2, ( #8821, #11208, #1551 ),
 .UNSPECIFIED., .F., .F. ) 
 B_SPLINE_CURVE_WITH_KNOTS ( ( 3, 3 ),
 ( 0.1168436138077930952, 0.2336872276155859962 ),
 .UNSPECIFIED. ) 
 CURVE ( )  GEOMETRIC_REPRESENTATION_ITEM ( )  RATIONAL_B_SPLINE_CURVE ( ( 1.077350269189629950, 1.077350269189629728, 1.000000000000000000 ) ) 
 REPRESENTATION_ITEM ( '' )  );
#5816=CARTESIAN_POINT ( 'NONE',  ( 28.07896398525729964, -3.287439373930340025, 11.50000000000019895 ) ) ;
#5865=ADVANCED_FACE ( 'NONE', ( #7529, #5732 ), #14537, .T. ) ;
#5872=EDGE_CURVE ( 'NONE', #11260, #10096, #16650, .T. ) ;
#5935=ORIENTED_EDGE ( 'NONE', *, *, #23032, .T. ) ;
#5979=FACE_OUTER_BOUND ( 'NONE', #14686, .T. ) ;
#6093=CARTESIAN_POINT ( 'NONE',  ( 28.67817383939640052, -0.7594070262926470027, 11.00000000000019895 ) ) ;
#6104=CARTESIAN_POINT ( 'NONE',  ( 31.11077410011089839, -1.335996977273150144, 11.00000000000019895 ) ) ;
#6141=ORIENTED_EDGE ( 'NONE', *, *, #17700, .T. ) ;
#6241=ORIENTED_EDGE ( 'NONE', *, *, #8628, .T. ) ;
#6273=ORIENTED_EDGE ( 'NONE', *, *, #10184, .T. ) ;
#6307=CIRCLE ( 'NONE', #19585, 2.600000000000000089 ) ;
#6404=CARTESIAN_POINT ( 'NONE',  ( 28.67817383939640052, -0.7594070262926470027, 11.00000000000019895 ) ) ;
#6457=CARTESIAN_POINT ( 'NONE',  ( 28.89837840081079889, -1.998294948772169954, 13.00000000000019895 ) ) ;
#6488=EDGE_CURVE ( 'NONE', #10685, #9733, #5771, .T. ) ;
#6513=ORIENTED_EDGE ( 'NONE', *, *, #11158, .F. ) ;
#6521=CARTESIAN_POINT ( 'NONE',  ( 52.73786095581300515, -7.648876468381139659, 10.99076000000024855 ) ) ;
#6601=AXIS2_PLACEMENT_3D ( 'NONE', #10444, #1607, #4950 ) ;
#6673=CARTESIAN_POINT ( 'NONE',  ( 52.26033179423370001, -7.535689554643850485, 13.00000000000019895 ) ) ;
#6706=APPLICATION_CONTEXT ( 'configuration controlled 3d designs of mechanical parts and assemblies' ) ;
#6708=CIRCLE ( 'NONE', #17708, 4.250000000000000000 ) ;
#6728=ADVANCED_FACE ( 'NONE', ( #21026 ), #3207, .T. ) ;
#6730=EDGE_CURVE ( 'NONE', #7581, #15508, #22840, .T. ) ;
#6742=ADVANCED_FACE ( 'NONE', ( #17592 ), #17241, .F. ) ;
#6839=CARTESIAN_POINT ( 'NONE',  ( 27.87922736721089834, -4.130116823142910398, 13.00000000000019895 ) ) ;
#6851=ORIENTED_EDGE ( 'NONE', *, *, #14300, .T. ) ;
#6922=ORIENTED_EDGE ( 'NONE', *, *, #2872, .T. ) ;
#7066=EDGE_CURVE ( 'NONE', #15508, #8933, #14821, .T. ) ;
#7145=ORIENTED_EDGE ( 'NONE', *, *, #22822, .T. ) ;
#7149=CARTESIAN_POINT ( 'NONE',  ( 28.14554285793940025, -3.006546890859489896, 15.00000000000000000 ) ) ;
#7222=ADVANCED_FACE ( 'NONE', ( #22864 ), #1242, .F. ) ;
#7255=ORIENTED_EDGE ( 'NONE', *, *, #1980, .F. ) ;
#7259=DIRECTION ( 'NONE',  ( 0.000000000000000000, 0.000000000000000000, 1.000000000000000000 ) ) ;
#7272=DIRECTION ( 'NONE',  ( 5.798605125234323991E-17, -1.374421231021384554E-17, 1.000000000000000000 ) ) ;
#7284=AXIS2_PLACEMENT_3D ( 'NONE', #12913, #9925, #17155 ) ;
#7299=VERTEX_POINT ( 'NONE', #8621 ) ;
#7387=EDGE_LOOP ( 'NONE', ( #19149, #4979, #16475, #10990, #21337 ) ) ;
#7389=ADVANCED_FACE ( 'NONE', ( #5275 ), #13029, .T. ) ;
#7432=LINE ( 'NONE', #3737, #19114 ) ;
#7529=FACE_BOUND ( 'NONE', #10320, .T. ) ;
#7580=ORIENTED_EDGE ( 'NONE', *, *, #11565, .F. ) ;
#7581=VERTEX_POINT ( 'NONE', #11601 ) ;
#7619=SHAPE_DEFINITION_REPRESENTATION ( #8918, #2509 ) ;
#7658=DIRECTION ( 'NONE',  ( -0.9730401042858036753, 0.2306359803922031493, 5.432877459303543355E-17 ) ) ;
#7681=CARTESIAN_POINT ( 'NONE',  ( 31.01827548281339375, -2.500766059351008153, 15.00000000000011369 ) ) ;
#7752=DIRECTION ( 'NONE',  ( -0.6880432561069586006, 0.1630842657209346236, 0.7071067811865459074 ) ) ;
#7767=EDGE_CURVE ( 'NONE', #8933, #1694, #22863, .T. ) ;
#7770=CIRCLE ( 'NONE', #9689, 0.5000000000000004441 ) ;
#7803=VERTEX_POINT ( 'NONE', #19364 ) ;
#7841=ORIENTED_EDGE ( 'NONE', *, *, #19138, .F. ) ;
#7884=CIRCLE ( 'NONE', #2578, 2.500000000000000444 ) ;
#7900=ORIENTED_EDGE ( 'NONE', *, *, #67, .F. ) ;
#7943=ADVANCED_BREP_SHAPE_REPRESENTATION ( '', ( #9215, #12739 ), #1146 ) ;
#7961=EDGE_LOOP ( 'NONE', ( #17953, #7145, #14701, #1294, #20366 ) ) ;
#7973=EDGE_CURVE ( 'NONE', #1408, #14586, #18052, .T. ) ;
#8122=ORIENTED_EDGE ( 'NONE', *, *, #7767, .F. ) ;
#8126=VECTOR ( 'NONE', #4034, 999.9999999999998863 ) ;
#8266=CIRCLE ( 'NONE', #13577, 2.600000000000000089 ) ;
#8286=CARTESIAN_POINT ( 'NONE',  ( 31.49315201223960159, -2.613324229818040134, 13.00000000000019895 ) ) ;
#8328=CARTESIAN_POINT ( 'NONE',  ( 31.37708959083939675, -0.2124270449897310287, 13.00000000000019895 ) ) ;
#8354=AXIS2_PLACEMENT_3D ( 'NONE', #4684, #13937, #21061 ) ;
#8386=CONICAL_SURFACE ( 'NONE', #19757, 1.154700538379250796, 1.047197551196598297 ) ;
#8387=CARTESIAN_POINT ( 'NONE',  ( 33.87671241911665021, -0.5062525893939895383, 13.00000000000019895 ) ) ;
#8396=VERTEX_POINT ( 'NONE', #12568 ) ;
#8439=DIRECTION ( 'NONE',  ( 0.000000000000000000, 1.734723475976806848E-16, 1.000000000000000000 ) ) ;
#8443=AXIS2_PLACEMENT_3D ( 'NONE', #8935, #19859, #22172 ) ;
#8459=CARTESIAN_POINT ( 'NONE',  ( 31.01827548281339375, -2.500766059351008153, 15.00000000000011546 ) ) ;
#8517=AXIS2_PLACEMENT_3D ( 'NONE', #6404, #13530, #22433 ) ;
#8530=CARTESIAN_POINT ( 'NONE',  ( 31.49315201223960159, -2.613324229818040134, 13.00000000000019895 ) ) ;
#8537=EDGE_CURVE ( 'NONE', #4472, #1408, #18498, .T. ) ;
#8574=ORIENTED_EDGE ( 'NONE', *, *, #17400, .F. ) ;
#8603=DIRECTION ( 'NONE',  ( 0.9730401042858035643, -0.2306359803922028717, -5.959266323858677443E-17 ) ) ;
#8621=CARTESIAN_POINT ( 'NONE',  ( 33.27705887009690144, -3.036156860537075453, 8.750000000000198952 ) ) ;
#8628=EDGE_CURVE ( 'NONE', #7581, #20636, #22115, .T. ) ;
#8684=CIRCLE ( 'NONE', #23072, 2.500000000000000444 ) ;
#8726=DIRECTION ( 'NONE',  ( -0.4865200521429014491, 0.1153179901961012555, 0.8660254037844388186 ) ) ;
#8729=AXIS2_PLACEMENT_3D ( 'NONE', #6457, #8603, #14055 ) ;
#8752=VERTEX_POINT ( 'NONE', #11627 ) ;
#8760=EDGE_CURVE ( 'NONE', #11069, #11256, #18550, .T. ) ;
#8821=CARTESIAN_POINT ( 'NONE',  ( 31.01827548281339020, -2.500766059351007708, 11.00000000000020428 ) ) ;
#8842=VECTOR ( 'NONE', #15955, 1000.000000000000000 ) ;
#8876=CIRCLE ( 'NONE', #1276, 0.5000000000000000000 ) ;
#8918=PRODUCT_DEFINITION_SHAPE ( 'NONE', 'NONE',  #19756 ) ;
#8933=VERTEX_POINT ( 'NONE', #20123 ) ;
#8935=CARTESIAN_POINT ( 'NONE',  ( 30.84445860938240003, -2.459566909556570202, 13.00000000000019895 ) ) ;
#9034=DIRECTION ( 'NONE',  ( 0.9730401042858035643, -0.2306359803922028717, -5.959266323858677443E-17 ) ) ;
#9051=EDGE_CURVE ( 'NONE', #4601, #3018, #19501, .T. ) ;
#9055=FACE_OUTER_BOUND ( 'NONE', #7387, .T. ) ;
#9124=APPLICATION_CONTEXT ( 'configuration controlled 3d designs of mechanical parts and assemblies' ) ;
#9154=ORIENTED_EDGE ( 'NONE', *, *, #2872, .F. ) ;
#9178=CARTESIAN_POINT ( 'NONE',  ( 31.11077410011089839, -1.335996977273150144, 15.00000000000000000 ) ) ;
#9210=DIRECTION ( 'NONE',  ( -0.9730401042858036753, 0.2306359803922028995, 5.959266323858677443E-17 ) ) ;
#9215=MANIFOLD_SOLID_BREP ( 'Imported1', #18556 ) ;
#9265=AXIS2_PLACEMENT_3D ( 'NONE', #18115, #16318, #14554 ) ;
#9271=EDGE_CURVE ( 'NONE', #22078, #12251, #18604, .T. ) ;
#9295=DIRECTION ( 'NONE',  ( -0.9730401042858036753, 0.2306359803922028995, 5.959266323858677443E-17 ) ) ;
#9324=DIRECTION ( 'NONE',  ( 0.1997366180463766849, 0.8426774492125652660, -0.5000000000000004441 ) ) ;
#9331=FACE_OUTER_BOUND ( 'NONE', #17216, .T. ) ;
#9358=CARTESIAN_POINT ( 'NONE',  ( 30.57814311865390167, -3.583136841839989817, 15.00000000000000000 ) ) ;
#9359=VECTOR ( 'NONE', #871, 1000.000000000000114 ) ;
#9375=( NAMED_UNIT ( * ) SI_UNIT ( $, .STERADIAN. ) SOLID_ANGLE_UNIT ( ) );
#9393=ORIENTED_EDGE ( 'NONE', *, *, #19192, .F. ) ;
#9425=ORIENTED_EDGE ( 'NONE', *, *, #12716, .T. ) ;
#9428=DIRECTION ( 'NONE',  ( -0.9730401042858036753, 0.2306359803922031493, 5.432877459303543355E-17 ) ) ;
#9437=PLANE ( 'NONE',  #1798 ) ;
#9445=CARTESIAN_POINT ( 'NONE',  ( 28.89837840081079889, -1.998294948772169954, 13.00000000000019895 ) ) ;
#9476=CARTESIAN_POINT ( 'NONE',  ( 33.27705887009690144, -3.036156860537075453, 17.25000000000019895 ) ) ;
#9482=ORIENTED_EDGE ( 'NONE', *, *, #12716, .F. ) ;
#9512=EDGE_CURVE ( 'NONE', #9733, #4472, #12851, .T. ) ;
#9567=CARTESIAN_POINT ( 'NONE',  ( 31.14187293219668717, -1.979315439058050297, 15.00000000000011724 ) ) ;
#9593=AXIS2_PLACEMENT_3D ( 'NONE', #22915, #15431, #20898 ) ;
#9655=DIRECTION ( 'NONE',  ( -0.9730401042858036753, 0.2306359803922031493, 5.432877459303543355E-17 ) ) ;
#9689=AXIS2_PLACEMENT_3D ( 'NONE', #13087, #7272, #12955 ) ;
#9703=ORIENTED_EDGE ( 'NONE', *, *, #14039, .T. ) ;
#9733=VERTEX_POINT ( 'NONE', #4524 ) ;
#9813=VECTOR ( 'NONE', #19978, 999.9999999999998863 ) ;
#9827=EDGE_CURVE ( 'NONE', #20287, #14097, #20206, .T. ) ;
#9889=CARTESIAN_POINT ( 'NONE',  ( 30.16078946048219933, 0.07586793050052280385, 13.00000000000019895 ) ) ;
#9925=DIRECTION ( 'NONE',  ( 0.9730401042858036753, -0.2306359803922031493, -5.959266323858673745E-17 ) ) ;
#9967=ORIENTED_EDGE ( 'NONE', *, *, #9271, .F. ) ;
#9990=VECTOR ( 'NONE', #565, 999.9999999999998863 ) ;
#10076=LINE ( 'NONE', #11857, #19006 ) ;
#10077=ORIENTED_EDGE ( 'NONE', *, *, #4585, .F. ) ;
#10090=ADVANCED_FACE ( 'NONE', ( #2817 ), #15280, .T. ) ;
#10096=VERTEX_POINT ( 'NONE', #4363 ) ;
#10098=EDGE_CURVE ( 'NONE', #22078, #8396, #13694, .T. ) ;
#10184=EDGE_CURVE ( 'NONE', #8396, #1694, #10076, .T. ) ;
#10231=( BOUNDED_CURVE ( )  B_SPLINE_CURVE ( 2, ( #11396, #18633, #2829 ),
 .UNSPECIFIED., .F., .F. ) 
 B_SPLINE_CURVE_WITH_KNOTS ( ( 3, 3 ),
 ( 0.000000000000000000, 0.2336872276155859962 ),
 .UNSPECIFIED. ) 
 CURVE ( )  GEOMETRIC_REPRESENTATION_ITEM ( )  RATIONAL_B_SPLINE_CURVE ( ( 1.000000000000000000, 1.154700538379259900, 1.000000000000000000 ) ) 
 REPRESENTATION_ITEM ( '' )  );
#10252=ORIENTED_EDGE ( 'NONE', *, *, #21315, .F. ) ;
#10259=CARTESIAN_POINT ( 'NONE',  ( 27.87922736721089834, -4.130116823142910398, 13.00000000000019895 ) ) ;
#10313=DIRECTION ( 'NONE',  ( -0.9730401042858035643, 0.2306359803922028717, 5.432877459303547053E-17 ) ) ;
#10317=LINE ( 'NONE', #3392, #4261 ) ;
#10320=EDGE_LOOP ( 'NONE', ( #19852, #4193, #5620, #18520, #1320, #5935 ) ) ;
#10337=DIRECTION ( 'NONE',  ( -0.2306359803922028440, -0.9730401042858034533, -4.307366329831518561E-32 ) ) ;
#10439=ORIENTED_EDGE ( 'NONE', *, *, #8537, .F. ) ;
#10444=CARTESIAN_POINT ( 'NONE',  ( 28.67817383939640052, -0.7594070262926440051, 15.00000000000000000 ) ) ;
#10446=EDGE_LOOP ( 'NONE', ( #8574, #20239, #10077, #9482, #10252 ) ) ;
#10475=CARTESIAN_POINT ( 'NONE',  ( 28.14554285793940025, -3.006546890859489896, 11.00000000000019895 ) ) ;
#10484=ORIENTED_EDGE ( 'NONE', *, *, #18394, .T. ) ;
#10509=CARTESIAN_POINT ( 'NONE',  ( 52.49909637502329929, -7.592283011512489743, 10.74538000000019800 ) ) ;
#10553=ORIENTED_EDGE ( 'NONE', *, *, #9827, .F. ) ;
#10561=ADVANCED_FACE ( 'NONE', ( #18363 ), #21788, .F. ) ;
#10598=FACE_OUTER_BOUND ( 'NONE', #584, .T. ) ;
#10609=ORIENTED_EDGE ( 'NONE', *, *, #18167, .F. ) ;
#10646=DIRECTION ( 'NONE',  ( 0.9730401042858035643, -0.2306359803922028717, -5.959266323858677443E-17 ) ) ;
#10685=VERTEX_POINT ( 'NONE', #4211 ) ;
#10732=DIRECTION ( 'NONE',  ( -0.9730401042858035643, 0.2306359803922028717, 5.667427308550587516E-17 ) ) ;
#10740=AXIS2_PLACEMENT_3D ( 'NONE', #10475, #4755, #21374 ) ;
#10755=ADVANCED_FACE ( 'NONE', ( #15839 ), #1499, .T. ) ;
#10786=AXIS2_PLACEMENT_3D ( 'NONE', #8286, #908, #15517 ) ;
#10943=DIRECTION ( 'NONE',  ( -0.9730401042858035643, 0.2306359803922028717, 6.126766849694256332E-17 ) ) ;
#10965=EDGE_LOOP ( 'NONE', ( #22533, #12182, #10439, #10972, #21168 ) ) ;
#10972=ORIENTED_EDGE ( 'NONE', *, *, #9512, .F. ) ;
#10990=ORIENTED_EDGE ( 'NONE', *, *, #10184, .F. ) ;
#11069=VERTEX_POINT ( 'NONE', #15222 ) ;
#11077=PRODUCT_DEFINITION_FORMATION_WITH_SPECIFIED_SOURCE ( 'ANY', '', #23309, .NOT_KNOWN. ) ;
#11101=CIRCLE ( 'NONE', #17555, 4.250000000000000000 ) ;
#11136=AXIS2_PLACEMENT_3D ( 'NONE', #5731, #16193, #1578 ) ;
#11158=EDGE_CURVE ( 'NONE', #18339, #18104, #18914, .T. ) ;
#11182=ORIENTED_EDGE ( 'NONE', *, *, #14612, .T. ) ;
#11208=CARTESIAN_POINT ( 'NONE',  ( 30.89467803343009678, -3.022216679643963566, 11.00000000000020606 ) ) ;
#11213=EDGE_CURVE ( 'NONE', #4601, #8933, #18566, .T. ) ;
#11216=MECHANICAL_CONTEXT ( 'NONE', #6706, 'mechanical' ) ;
#11248=DIRECTION ( 'NONE',  ( -0.9286452767786568252, -1.871119812896369614E-17, -0.3709689338970204586 ) ) ;
#11253=ORIENTED_EDGE ( 'NONE', *, *, #20637, .F. ) ;
#11256=VERTEX_POINT ( 'NONE', #8459 ) ;
#11260=VERTEX_POINT ( 'NONE', #12146 ) ;
#11396=CARTESIAN_POINT ( 'NONE',  ( 30.57814311865390167, -3.583136841839989817, 11.00000000000019895 ) ) ;
#11565=EDGE_CURVE ( 'NONE', #3018, #4601, #3316, .T. ) ;
#11582=CARTESIAN_POINT ( 'NONE',  ( 28.14554285793940025, -3.006546890859489896, 11.00000000000019895 ) ) ;
#11601=CARTESIAN_POINT ( 'NONE',  ( 32.79777292954499757, -5.491820719290810615, 13.00000000000019895 ) ) ;
#11606=LINE ( 'NONE', #16660, #18524 ) ;
#11627=CARTESIAN_POINT ( 'NONE',  ( 29.27674327513866004, 1.765923432495702716, 13.00000000000019895 ) ) ;
#11632=DIRECTION ( 'NONE',  ( 0.000000000000000000, 1.734723475976806848E-16, 1.000000000000000000 ) ) ;
#11638=FACE_OUTER_BOUND ( 'NONE', #14911, .T. ) ;
#11757=( BOUNDED_CURVE ( )  B_SPLINE_CURVE ( 2, ( #16085, #23316, #11965 ),
 .UNSPECIFIED., .F., .F. ) 
 B_SPLINE_CURVE_WITH_KNOTS ( ( 3, 3 ),
 ( 0.000000000000000000, 0.1168436138077930952 ),
 .UNSPECIFIED. ) 
 CURVE ( )  GEOMETRIC_REPRESENTATION_ITEM ( )  RATIONAL_B_SPLINE_CURVE ( ( 1.000000000000000000, 1.077350269189630172, 1.077350269189629950 ) ) 
 REPRESENTATION_ITEM ( '' )  );
#11776=ORIENTED_EDGE ( 'NONE', *, *, #17400, .T. ) ;
#11819=AXIS2_PLACEMENT_3D ( 'NONE', #17053, #663, #20736 ) ;
#11840=VERTEX_POINT ( 'NONE', #12119 ) ;
#11857=CARTESIAN_POINT ( 'NONE',  ( 43.98050001724080005, -5.573152644851309567, 10.50000000000019895 ) ) ;
#11965=CARTESIAN_POINT ( 'NONE',  ( 31.01827548281339020, -2.500766059351007708, 11.00000000000020428 ) ) ;
#11970=DIRECTION ( 'NONE',  ( 0.000000000000000000, 1.020425574104004122E-16, 1.000000000000000000 ) ) ;
#12084=CARTESIAN_POINT ( 'NONE',  ( 33.95095283150600807, -0.6266201978617900181, 13.00000000000019895 ) ) ;
#12103=EDGE_LOOP ( 'NONE', ( #13228, #10484, #22599, #5615, #5638 ) ) ;
#12119=CARTESIAN_POINT ( 'NONE',  ( 27.54697342219713718, -5.531877349647827735, 13.00000000000019895 ) ) ;
#12146=CARTESIAN_POINT ( 'NONE',  ( 28.89837840081079889, -1.998294948772166180, 8.750000000000198952 ) ) ;
#12172=LINE ( 'NONE', #17144, #9813 ) ;
#12182=ORIENTED_EDGE ( 'NONE', *, *, #67, .T. ) ;
#12251=VERTEX_POINT ( 'NONE', #8387 ) ;
#12252=CARTESIAN_POINT ( 'NONE',  ( 33.37436288052550282, -3.059220458576299873, 13.00000000000019895 ) ) ;
#12284=DIRECTION ( 'NONE',  ( -0.9730401042858036753, 0.2306359803922028995, 5.959266323858677443E-17 ) ) ;
#12438=FACE_OUTER_BOUND ( 'NONE', #21738, .T. ) ;
#12517=ADVANCED_FACE ( 'NONE', ( #271 ), #9437, .F. ) ;
#12520=ORIENTED_EDGE ( 'NONE', *, *, #20167, .T. ) ;
#12540=DIRECTION ( 'NONE',  ( -0.9730401042858035643, 0.2306359803922028717, 6.126766849694256332E-17 ) ) ;
#12568=CARTESIAN_POINT ( 'NONE',  ( 33.37436288052550992, -3.059220458576291435, 10.50000000000019895 ) ) ;
#12571=EDGE_CURVE ( 'NONE', #20636, #12251, #8266, .T. ) ;
#12689=DIRECTION ( 'NONE',  ( 0.2306359803922028995, 0.9730401042858036753, -9.756037151021835575E-16 ) ) ;
#12716=EDGE_CURVE ( 'NONE', #11260, #7299, #12172, .T. ) ;
#12739=AXIS2_PLACEMENT_3D ( 'NONE', #2569, #13380, #415 ) ;
#12828=ADVANCED_FACE ( 'NONE', ( #9055 ), #16287, .T. ) ;
#12851=LINE ( 'NONE', #3814, #16672 ) ;
#12862=VERTEX_POINT ( 'NONE', #21757 ) ;
#12913=CARTESIAN_POINT ( 'NONE',  ( 28.41185834866789861, -1.882976958576060067, 13.00000000000019895 ) ) ;
#12952=ORIENTED_EDGE ( 'NONE', *, *, #8760, .T. ) ;
#12955=DIRECTION ( 'NONE',  ( 1.000000000000000000, 0.000000000000000000, 0.000000000000000000 ) ) ;
#12969=CIRCLE ( 'NONE', #7284, 3.750000000000000000 ) ;
#12987=DIRECTION ( 'NONE',  ( 6.124378941433959925E-17, 0.000000000000000000, 1.000000000000000000 ) ) ;
#13029=TOROIDAL_SURFACE ( 'NONE', #23247, 3.750000000000000000, 0.5000000000000000000 ) ;
#13087=CARTESIAN_POINT ( 'NONE',  ( 28.03349347434003747, -5.647195339843935180, 13.00000000000019895 ) ) ;
#13119=EDGE_CURVE ( 'NONE', #1694, #8933, #8684, .T. ) ;
#13124=CARTESIAN_POINT ( 'NONE',  ( 31.11077410011089839, -1.335996977273150144, 15.00000000000000000 ) ) ;
#13197=AXIS2_PLACEMENT_3D ( 'NONE', #1205, #13349, #20705 ) ;
#13216=DIRECTION ( 'NONE',  ( 0.9730401042858036753, -0.2306359803922031493, -5.432877459303553216E-17 ) ) ;
#13218=DIRECTION ( 'NONE',  ( 0.9730401042858036753, -0.2306359803922028995, -5.432877459303547669E-17 ) ) ;
#13228=ORIENTED_EDGE ( 'NONE', *, *, #15657, .T. ) ;
#13263=ORIENTED_EDGE ( 'NONE', *, *, #23032, .F. ) ;
#13265=DIRECTION ( 'NONE',  ( -0.9730401042858035643, 0.2306359803922028717, 6.126766849694256332E-17 ) ) ;
#13349=DIRECTION ( 'NONE',  ( 0.9730401042858035643, -0.2306359803922028717, -5.959266323858674978E-17 ) ) ;
#13380=DIRECTION ( 'NONE',  ( 0.000000000000000000, 0.000000000000000000, 1.000000000000000000 ) ) ;
#13448=DIRECTION ( 'NONE',  ( 0.9730401042858035643, -0.2306359803922028717, -5.432877459303547053E-17 ) ) ;
#13530=DIRECTION ( 'NONE',  ( -2.829953705592110306E-16, -9.355573283744330345E-16, -1.000000000000000000 ) ) ;
#13544=DIRECTION ( 'NONE',  ( 0.9730401042858035643, -0.2306359803922028717, -5.959266323858667582E-17 ) ) ;
#13577=AXIS2_PLACEMENT_3D ( 'NONE', #1210, #19173, #17272 ) ;
#13671=AXIS2_PLACEMENT_3D ( 'NONE', #550, #13265, #11632 ) ;
#13694=CIRCLE ( 'NONE', #13671, 2.500000000000000444 ) ;
#13738=ORIENTED_EDGE ( 'NONE', *, *, #12571, .F. ) ;
#13762=EDGE_CURVE ( 'NONE', #8396, #7581, #7884, .T. ) ;
#13771=ORIENTED_EDGE ( 'NONE', *, *, #9827, .T. ) ;
#13916=DIRECTION ( 'NONE',  ( 0.9730401042858036753, -0.2306359803922031493, -5.432877459303553216E-17 ) ) ;
#13937=DIRECTION ( 'NONE',  ( -8.623081276789554834E-17, -1.054188326053478339E-16, -1.000000000000000000 ) ) ;
#14039=EDGE_CURVE ( 'NONE', #11256, #14790, #3812, .T. ) ;
#14055=DIRECTION ( 'NONE',  ( -0.2306359803922028995, -0.9730401042858035643, -1.064172857958375654E-32 ) ) ;
#14075=EDGE_CURVE ( 'NONE', #7803, #16383, #11606, .T. ) ;
#14097=VERTEX_POINT ( 'NONE', #6104 ) ;
#14226=VECTOR ( 'NONE', #20758, 1000.000000000000114 ) ;
#14300=EDGE_CURVE ( 'NONE', #3018, #1694, #3243, .T. ) ;
#14350=ORIENTED_EDGE ( 'NONE', *, *, #9051, .T. ) ;
#14382=ORIENTED_EDGE ( 'NONE', *, *, #18167, .T. ) ;
#14392=AXIS2_PLACEMENT_3D ( 'NONE', #19760, #9428, #3717 ) ;
#14537=PLANE ( 'NONE',  #2248 ) ;
#14554=DIRECTION ( 'NONE',  ( 0.000000000000000000, 0.000000000000000000, 1.000000000000000000 ) ) ;
#14586=VERTEX_POINT ( 'NONE', #22106 ) ;
#14612=EDGE_CURVE ( 'NONE', #18104, #7299, #5190, .T. ) ;
#14628=CARTESIAN_POINT ( 'NONE',  ( 28.89837840081079889, -1.998294948772169954, 13.00000000000019895 ) ) ;
#14686=EDGE_LOOP ( 'NONE', ( #22341, #2615, #15762, #20110 ) ) ;
#14701=ORIENTED_EDGE ( 'NONE', *, *, #9271, .T. ) ;
#14786=CARTESIAN_POINT ( 'NONE',  ( 33.27705887009690144, -3.036156860537079893, 9.625000000000159872 ) ) ;
#14789=LINE ( 'NONE', #3864, #19459 ) ;
#14790=VERTEX_POINT ( 'NONE', #17468 ) ;
#14821=LINE ( 'NONE', #439, #9990 ) ;
#14842=EDGE_CURVE ( 'NONE', #14586, #20287, #2633, .T. ) ;
#14850=AXIS2_PLACEMENT_3D ( 'NONE', #20767, #4498, #10337 ) ;
#14852=VECTOR ( 'NONE', #12284, 999.9999999999998863 ) ;
#14896=DIRECTION ( 'NONE',  ( -0.2306359803922028995, -0.9730401042858036753, 1.343075398093749487E-16 ) ) ;
#14903=DIRECTION ( 'NONE',  ( 0.000000000000000000, 1.020425574104004122E-16, 1.000000000000000000 ) ) ;
#14907=VECTOR ( 'NONE', #3608, 1000.000000000000114 ) ;
#14911=EDGE_LOOP ( 'NONE', ( #3894, #20064, #9703, #6922, #13771, #4238 ) ) ;
#14973=ADVANCED_FACE ( 'NONE', ( #10598 ), #15835, .F. ) ;
#15222=CARTESIAN_POINT ( 'NONE',  ( 30.57814311865390167, -3.583136841839989817, 15.00000000000000000 ) ) ;
#15280=CYLINDRICAL_SURFACE ( 'NONE', #11819, 2.500000000000000444 ) ;
#15360=ADVANCED_FACE ( 'NONE', ( #19337 ), #3089, .F. ) ;
#15431=DIRECTION ( 'NONE',  ( 0.9730401042858035643, -0.2306359803922028717, -5.432877459303547053E-17 ) ) ;
#15508=VERTEX_POINT ( 'NONE', #17688 ) ;
#15517=DIRECTION ( 'NONE',  ( 0.000000000000000000, 0.000000000000000000, -1.000000000000000000 ) ) ;
#15618=DIRECTION ( 'NONE',  ( -0.9730401042858036753, 0.2306359803922031493, 5.432877459303543355E-17 ) ) ;
#15657=EDGE_CURVE ( 'NONE', #11840, #8752, #12969, .T. ) ;
#15754=ORIENTED_EDGE ( 'NONE', *, *, #10098, .T. ) ;
#15762=ORIENTED_EDGE ( 'NONE', *, *, #11213, .T. ) ;
#15828=( BOUNDED_CURVE ( )  B_SPLINE_CURVE ( 2, ( #3657, #18275, #9358 ),
 .UNSPECIFIED., .F., .F. ) 
 B_SPLINE_CURVE_WITH_KNOTS ( ( 3, 3 ),
 ( 0.000000000000000000, 0.2336872276155859962 ),
 .UNSPECIFIED. ) 
 CURVE ( )  GEOMETRIC_REPRESENTATION_ITEM ( )  RATIONAL_B_SPLINE_CURVE ( ( 1.000000000000000000, 1.154700538379249908, 1.000000000000000000 ) ) 
 REPRESENTATION_ITEM ( '' )  );
#15835=TOROIDAL_SURFACE ( 'NONE', #19245, 2.600000000000000089, 0.1000000000000000056 ) ;
#15839=FACE_OUTER_BOUND ( 'NONE', #4001, .T. ) ;
#15925=CARTESIAN_POINT ( 'NONE',  ( 52.73786095581300515, -7.648876468381139659, 15.00924000000014935 ) ) ;
#15955=DIRECTION ( 'NONE',  ( -0.4865200521429013936, 0.1153179901961013387, -0.8660254037844388186 ) ) ;
#16052=CYLINDRICAL_SURFACE ( 'NONE', #8443, 4.250000000000000000 ) ;
#16085=CARTESIAN_POINT ( 'NONE',  ( 31.11077410011089839, -1.335996977273150144, 11.00000000000019895 ) ) ;
#16101=DESIGN_CONTEXT ( 'detailed design', #9124, 'design' ) ;
#16119=CIRCLE ( 'NONE', #182, 2.500000000000000444 ) ;
#16149=CARTESIAN_POINT ( 'NONE',  ( 33.37436288052550282, -3.059220458576299873, 13.00000000000019895 ) ) ;
#16150=ORIENTED_EDGE ( 'NONE', *, *, #18394, .F. ) ;
#16158=ORIENTED_EDGE ( 'NONE', *, *, #14842, .T. ) ;
#16193=DIRECTION ( 'NONE',  ( 0.9730401042858036753, -0.2306359803922031493, -5.959266323858673745E-17 ) ) ;
#16287=CYLINDRICAL_SURFACE ( 'NONE', #1444, 2.500000000000000444 ) ;
#16318=DIRECTION ( 'NONE',  ( -0.9730401042858035643, 0.2306359803922028717, 5.959266323858677443E-17 ) ) ;
#16379=CARTESIAN_POINT ( 'NONE',  ( 28.87791045744280183, 0.08327042291992099721, 12.50000000000020073 ) ) ;
#16383=VERTEX_POINT ( 'NONE', #7149 ) ;
#16394=CONICAL_SURFACE ( 'NONE', #3499, 2.254620000000000513, 0.7853981633974461696 ) ;
#16447=PLANE ( 'NONE',  #17565 ) ;
#16475=ORIENTED_EDGE ( 'NONE', *, *, #13119, .F. ) ;
#16568=AXIS2_PLACEMENT_3D ( 'NONE', #19721, #3448, #7259 ) ;
#16603=ORIENTED_EDGE ( 'NONE', *, *, #17226, .T. ) ;
#16650=CIRCLE ( 'NONE', #14392, 4.250000000000000000 ) ;
#16660=CARTESIAN_POINT ( 'NONE',  ( 28.27870060330370094, -2.444761924717779866, 15.00000000000000000 ) ) ;
#16672=VECTOR ( 'NONE', #9295, 999.9999999999998863 ) ;
#16744=DIRECTION ( 'NONE',  ( 0.000000000000000000, 1.020425574104004122E-16, 1.000000000000000000 ) ) ;
#16842=FACE_OUTER_BOUND ( 'NONE', #10446, .T. ) ;
#17053=CARTESIAN_POINT ( 'NONE',  ( 43.98050001724080005, -5.573152644851309567, 13.00000000000019895 ) ) ;
#17117=CARTESIAN_POINT ( 'NONE',  ( 31.56827854690379098, -0.8510906712621758574, 12.00000000000019185 ) ) ;
#17144=CARTESIAN_POINT ( 'NONE',  ( 30.84445860938240003, -2.459566909556570202, 8.750000000000198952 ) ) ;
#17155=DIRECTION ( 'NONE',  ( 0.000000000000000000, 1.156482317317871478E-16, 1.000000000000000000 ) ) ;
#17216=EDGE_LOOP ( 'NONE', ( #22904, #11182 ) ) ;
#17226=EDGE_CURVE ( 'NONE', #306, #19524, #7432, .T. ) ;
#17232=EDGE_LOOP ( 'NONE', ( #6513, #327, #22036, #9425, #3049 ) ) ;
#17241=PLANE ( 'NONE',  #10740 ) ;
#17259=DIRECTION ( 'NONE',  ( 0.000000000000000000, 0.000000000000000000, -1.000000000000000000 ) ) ;
#17272=DIRECTION ( 'NONE',  ( 0.000000000000000000, 1.668003342285391304E-16, 1.000000000000000000 ) ) ;
#17336=FACE_OUTER_BOUND ( 'NONE', #10965, .T. ) ;
#17377=ORIENTED_EDGE ( 'NONE', *, *, #7066, .F. ) ;
#17400=EDGE_CURVE ( 'NONE', #18339, #4805, #1274, .T. ) ;
#17409=CARTESIAN_POINT ( 'NONE',  ( 28.89837840081079889, -1.998294948772169954, 13.00000000000019895 ) ) ;
#17468=CARTESIAN_POINT ( 'NONE',  ( 31.11077410011089839, -1.335996977273150144, 15.00000000000000000 ) ) ;
#17550=DIRECTION ( 'NONE',  ( -0.1153179901961009640, -0.4865200521429018377, 0.8660254037844385966 ) ) ;
#17555=AXIS2_PLACEMENT_3D ( 'NONE', #4892, #13916, #17259 ) ;
#17565=AXIS2_PLACEMENT_3D ( 'NONE', #14786, #3860, #169 ) ;
#17592=FACE_OUTER_BOUND ( 'NONE', #4234, .T. ) ;
#17688=CARTESIAN_POINT ( 'NONE',  ( 33.37436288052550992, -3.059220458576291435, 15.50000000000019895 ) ) ;
#17700=EDGE_CURVE ( 'NONE', #11069, #16383, #20062, .T. ) ;
#17708=AXIS2_PLACEMENT_3D ( 'NONE', #14628, #9655, #16744 ) ;
#17756=CARTESIAN_POINT ( 'NONE',  ( 32.67740532107718820, -5.566061131680170249, 13.00000000000019895 ) ) ;
#17827=ADVANCED_FACE ( 'NONE', ( #17336 ), #20539, .F. ) ;
#17863=LINE ( 'NONE', #5383, #14907 ) ;
#17953=ORIENTED_EDGE ( 'NONE', *, *, #6730, .T. ) ;
#17962=ORIENTED_EDGE ( 'NONE', *, *, #15657, .F. ) ;
#17981=CARTESIAN_POINT ( 'NONE',  ( 43.98050001724080005, -5.573152644851309567, 13.00000000000019895 ) ) ;
#18052=LINE ( 'NONE', #16379, #19467 ) ;
#18104=VERTEX_POINT ( 'NONE', #9476 ) ;
#18109=AXIS2_PLACEMENT_3D ( 'NONE', #622, #5514, #21780 ) ;
#18115=CARTESIAN_POINT ( 'NONE',  ( 52.73786095581300515, -7.648876468381129889, 13.00000000000019895 ) ) ;
#18129=ORIENTED_EDGE ( 'NONE', *, *, #8760, .F. ) ;
#18167=EDGE_CURVE ( 'NONE', #306, #11069, #15828, .T. ) ;
#18230=DIRECTION ( 'NONE',  ( 0.000000000000000000, 1.734723475976806848E-16, 1.000000000000000000 ) ) ;
#18258=AXIS2_PLACEMENT_3D ( 'NONE', #2073, #9324, #11248 ) ;
#18275=CARTESIAN_POINT ( 'NONE',  ( 30.76933207471829590, -4.221800468112435922, 14.00000000000021672 ) ) ;
#18339=VERTEX_POINT ( 'NONE', #22630 ) ;
#18355=DIRECTION ( 'NONE',  ( -0.2306359803922028995, -0.9730401042858035643, -1.064172857958375654E-32 ) ) ;
#18363=FACE_OUTER_BOUND ( 'NONE', #3827, .T. ) ;
#18367=ADVANCED_FACE ( 'NONE', ( #11638 ), #1643, .F. ) ;
#18369=FACE_BOUND ( 'NONE', #2939, .T. ) ;
#18394=EDGE_CURVE ( 'NONE', #8752, #4805, #8876, .T. ) ;
#18439=EDGE_CURVE ( 'NONE', #14586, #7803, #10317, .T. ) ;
#18472=AXIS2_PLACEMENT_3D ( 'NONE', #20567, #13216, #20448 ) ;
#18498=LINE ( 'NONE', #2211, #5085 ) ;
#18511=ADVANCED_FACE ( 'NONE', ( #12438 ), #21208, .F. ) ;
#18520=ORIENTED_EDGE ( 'NONE', *, *, #14075, .T. ) ;
#18524=VECTOR ( 'NONE', #14896, 999.9999999999998863 ) ;
#18550=( BOUNDED_CURVE ( )  B_SPLINE_CURVE ( 2, ( #2686, #419, #7681 ),
 .UNSPECIFIED., .F., .F. ) 
 B_SPLINE_CURVE_WITH_KNOTS ( ( 3, 3 ),
 ( 0.000000000000000000, 0.1168436138077928454 ),
 .UNSPECIFIED. ) 
 CURVE ( )  GEOMETRIC_REPRESENTATION_ITEM ( )  RATIONAL_B_SPLINE_CURVE ( ( 1.000000000000000000, 1.077350269189624843, 1.077350269189624843 ) ) 
 REPRESENTATION_ITEM ( '' )  );
#18556=CLOSED_SHELL ( 'NONE', ( #18367, #19694, #7389, #19684, #12828, #15360, #14973, #10090, #18708, #22489, #22614, #10755, #5865, #6728, #7222, #6742, #17827, #10561, #12517, #18511, #3619 ) ) ;
#18566=LINE ( 'NONE', #494, #21495 ) ;
#18604=CIRCLE ( 'NONE', #8354, 0.09999999999999999167 ) ;
#18628=DIRECTION ( 'NONE',  ( -8.623081276789554834E-17, -1.054188326053478339E-16, -1.000000000000000000 ) ) ;
#18633=CARTESIAN_POINT ( 'NONE',  ( 30.76933207471829945, -4.221800468112443916, 12.00000000000019185 ) ) ;
#18708=ADVANCED_FACE ( 'NONE', ( #9331, #18369 ), #16447, .T. ) ;
#18895=EDGE_LOOP ( 'NONE', ( #17962, #7841 ) ) ;
#18914=LINE ( 'NONE', #4180, #22252 ) ;
#19006=VECTOR ( 'NONE', #19095, 999.9999999999998863 ) ;
#19095=DIRECTION ( 'NONE',  ( 0.9730401042858036753, -0.2306359803922028995, -5.432877459303547669E-17 ) ) ;
#19114=VECTOR ( 'NONE', #9210, 999.9999999999998863 ) ;
#19138=EDGE_CURVE ( 'NONE', #8752, #11840, #22482, .T. ) ;
#19149=ORIENTED_EDGE ( 'NONE', *, *, #22822, .F. ) ;
#19152=ORIENTED_EDGE ( 'NONE', *, *, #13762, .F. ) ;
#19173=DIRECTION ( 'NONE',  ( 0.9730401042858035643, -0.2306359803922028717, -5.959266323858667582E-17 ) ) ;
#19192=EDGE_CURVE ( 'NONE', #16383, #19524, #17863, .T. ) ;
#19245=AXIS2_PLACEMENT_3D ( 'NONE', #16149, #9034, #23381 ) ;
#19273=CARTESIAN_POINT ( 'NONE',  ( 29.89447396975369742, -1.047702001782899961, 11.00000000000019895 ) ) ;
#19308=DIRECTION ( 'NONE',  ( -0.9730401042858036753, 0.2306359803922023999, -1.110223024625155524E-17 ) ) ;
#19337=FACE_OUTER_BOUND ( 'NONE', #7961, .T. ) ;
#19364=CARTESIAN_POINT ( 'NONE',  ( 28.67817383939640052, -0.7594070262926440051, 15.00000000000000000 ) ) ;
#19367=CARTESIAN_POINT ( 'NONE',  ( 31.11077410011089839, -1.335996977273150144, 11.00000000000019895 ) ) ;
#19442=ORIENTED_EDGE ( 'NONE', *, *, #19814, .T. ) ;
#19459=VECTOR ( 'NONE', #3986, 999.9999999999998863 ) ;
#19467=VECTOR ( 'NONE', #100, 1000.000000000000114 ) ;
#19482=DIRECTION ( 'NONE',  ( -0.9730401042858035643, 0.2306359803922028717, 6.126766849694256332E-17 ) ) ;
#19488=CARTESIAN_POINT ( 'NONE',  ( 52.26033179423370001, -7.535689554643850485, 13.00000000000019895 ) ) ;
#19501=CIRCLE ( 'NONE', #9265, 2.009239999999998805 ) ;
#19524=VERTEX_POINT ( 'NONE', #10259 ) ;
#19585=AXIS2_PLACEMENT_3D ( 'NONE', #22561, #13544, #20786 ) ;
#19684=ADVANCED_FACE ( 'NONE', ( #2224 ), #16394, .T. ) ;
#19689=DIRECTION ( 'NONE',  ( 0.000000000000000000, 0.000000000000000000, 1.000000000000000000 ) ) ;
#19693=ORIENTED_EDGE ( 'NONE', *, *, #22096, .T. ) ;
#19694=ADVANCED_FACE ( 'NONE', ( #16842 ), #16052, .T. ) ;
#19721=CARTESIAN_POINT ( 'NONE',  ( 52.73786095581300515, -7.648876468381129889, 13.00000000000019895 ) ) ;
#19756=PRODUCT_DEFINITION ( 'UNKNOWN', '', #11077, #16101 ) ;
#19757=AXIS2_PLACEMENT_3D ( 'NONE', #8530, #10313, #1604 ) ;
#19760=CARTESIAN_POINT ( 'NONE',  ( 28.89837840081079889, -1.998294948772169954, 13.00000000000019895 ) ) ;
#19770=CARTESIAN_POINT ( 'NONE',  ( 28.89837840081079889, -1.998294948772169954, 13.00000000000019895 ) ) ;
#19814=EDGE_CURVE ( 'NONE', #9733, #306, #10231, .T. ) ;
#19840=ORIENTED_EDGE ( 'NONE', *, *, #13762, .T. ) ;
#19852=ORIENTED_EDGE ( 'NONE', *, *, #8537, .T. ) ;
#19859=DIRECTION ( 'NONE',  ( 0.9730401042858035643, -0.2306359803922028717, -5.432877459303547053E-17 ) ) ;
#19948=( LENGTH_UNIT ( ) NAMED_UNIT ( * ) SI_UNIT ( .MILLI., .METRE. ) );
#19978=DIRECTION ( 'NONE',  ( 0.9730401042858036753, -0.2306359803922028995, -5.432877459303547669E-17 ) ) ;
#19983=AXIS2_PLACEMENT_3D ( 'NONE', #17409, #15618, #11970 ) ;
#20062=LINE ( 'NONE', #220, #8126 ) ;
#20064=ORIENTED_EDGE ( 'NONE', *, *, #20637, .T. ) ;
#20110=ORIENTED_EDGE ( 'NONE', *, *, #7767, .T. ) ;
#20123=CARTESIAN_POINT ( 'NONE',  ( 52.26033179423370001, -7.535689554643851373, 15.50000000000019895 ) ) ;
#20136=EDGE_LOOP ( 'NONE', ( #11253, #923, #2220, #19442, #14382, #12952 ) ) ;
#20167=EDGE_CURVE ( 'NONE', #14790, #7803, #14789, .T. ) ;
#20206=( BOUNDED_CURVE ( )  B_SPLINE_CURVE ( 2, ( #8328, #17117, #19367 ),
 .UNSPECIFIED., .F., .F. ) 
 B_SPLINE_CURVE_WITH_KNOTS ( ( 3, 3 ),
 ( 0.000000000000000000, 0.2336872276155859962 ),
 .UNSPECIFIED. ) 
 CURVE ( )  GEOMETRIC_REPRESENTATION_ITEM ( )  RATIONAL_B_SPLINE_CURVE ( ( 1.000000000000000000, 1.154700538379259900, 1.000000000000000000 ) ) 
 REPRESENTATION_ITEM ( '' )  );
#20212=CARTESIAN_POINT ( 'NONE',  ( 52.26033179423370001, -7.535689554643851373, 10.50000000000019895 ) ) ;
#20239=ORIENTED_EDGE ( 'NONE', *, *, #11158, .T. ) ;
#20287=VERTEX_POINT ( 'NONE', #21911 ) ;
#20317=ORIENTED_EDGE ( 'NONE', *, *, #20167, .F. ) ;
#20366=ORIENTED_EDGE ( 'NONE', *, *, #8628, .F. ) ;
#20448=DIRECTION ( 'NONE',  ( 0.000000000000000000, 0.000000000000000000, -1.000000000000000000 ) ) ;
#20539=PLANE ( 'NONE',  #8517 ) ;
#20567=CARTESIAN_POINT ( 'NONE',  ( 33.27705887009690144, -3.036156860537079893, 13.00000000000019895 ) ) ;
#20636=VERTEX_POINT ( 'NONE', #17756 ) ;
#20637=EDGE_CURVE ( 'NONE', #12862, #11256, #3148, .T. ) ;
#20650=ORIENTED_EDGE ( 'NONE', *, *, #7973, .F. ) ;
#20669=EDGE_CURVE ( 'NONE', #14097, #10685, #11757, .T. ) ;
#20705=DIRECTION ( 'NONE',  ( -9.594916218540590128E-33, 2.583840697242805182E-16, -1.000000000000000000 ) ) ;
#20736=DIRECTION ( 'NONE',  ( 0.000000000000000000, 0.000000000000000000, -1.000000000000000000 ) ) ;
#20758=DIRECTION ( 'NONE',  ( 0.1153179901961009640, 0.4865200521429018377, -0.8660254037844385966 ) ) ;
#20767=CARTESIAN_POINT ( 'NONE',  ( 33.37436288052550282, -3.059220458576299873, 13.00000000000019895 ) ) ;
#20786=DIRECTION ( 'NONE',  ( 0.000000000000000000, 1.668003342285391304E-16, 1.000000000000000000 ) ) ;
#20844=DIRECTION ( 'NONE',  ( -0.1997366180463769070, -0.8426774492125652660, 0.5000000000000002220 ) ) ;
#20849=CARTESIAN_POINT ( 'NONE',  ( 32.77470933150577537, -5.589124729719389784, 13.00000000000019895 ) ) ;
#20898=DIRECTION ( 'NONE',  ( 0.000000000000000000, 0.000000000000000000, -1.000000000000000000 ) ) ;
#21026=FACE_OUTER_BOUND ( 'NONE', #17232, .T. ) ;
#21061=DIRECTION ( 'NONE',  ( 0.000000000000000000, 1.000000000000000000, 0.000000000000000000 ) ) ;
#21137=DIRECTION ( 'NONE',  ( 0.000000000000000000, 0.000000000000000000, 1.000000000000000000 ) ) ;
#21168=ORIENTED_EDGE ( 'NONE', *, *, #6488, .F. ) ;
#21208=PLANE ( 'NONE',  #6601 ) ;
#21315=EDGE_CURVE ( 'NONE', #4805, #11260, #6708, .T. ) ;
#21337=ORIENTED_EDGE ( 'NONE', *, *, #10098, .F. ) ;
#21374=DIRECTION ( 'NONE',  ( 0.000000000000000000, 0.5102823824563427202, -0.8600069128528436968 ) ) ;
#21391=ORIENTED_EDGE ( 'NONE', *, *, #215, .T. ) ;
#21495=VECTOR ( 'NONE', #7752, 1000.000000000000114 ) ;
#21661=EDGE_LOOP ( 'NONE', ( #150, #7580 ) ) ;
#21719=( NAMED_UNIT ( * ) PLANE_ANGLE_UNIT ( ) SI_UNIT ( $, .RADIAN. ) );
#21738=EDGE_LOOP ( 'NONE', ( #9154, #12520, #5012, #16158 ) ) ;
#21757=CARTESIAN_POINT ( 'NONE',  ( 32.14184541509679605, -2.767081550079510510, 13.00000000000019895 ) ) ;
#21780=DIRECTION ( 'NONE',  ( 0.000000000000000000, 0.000000000000000000, 1.000000000000000000 ) ) ;
#21788=PLANE ( 'NONE',  #18258 ) ;
#21845=CARTESIAN_POINT ( 'NONE',  ( 29.87858131747766421, 2.137125494442494222, 13.00000000000019895 ) ) ;
#21911=CARTESIAN_POINT ( 'NONE',  ( 31.37708959083939675, -0.2124270449897310287, 13.00000000000019895 ) ) ;
#21931=ORIENTED_EDGE ( 'NONE', *, *, #11213, .F. ) ;
#21940=DIRECTION ( 'NONE',  ( 0.000000000000000000, 1.734723475976806848E-16, 1.000000000000000000 ) ) ;
#21993=DIRECTION ( 'NONE',  ( -0.9730401042858035643, 0.2306359803922028717, 5.959266323858679908E-17 ) ) ;
#22036=ORIENTED_EDGE ( 'NONE', *, *, #5872, .F. ) ;
#22078=VERTEX_POINT ( 'NONE', #12084 ) ;
#22096=EDGE_CURVE ( 'NONE', #10096, #18339, #1391, .T. ) ;
#22106=CARTESIAN_POINT ( 'NONE',  ( 28.94448933012489888, 0.3641629059907759425, 13.00000000000019895 ) ) ;
#22115=CIRCLE ( 'NONE', #893, 0.1000000000000028644 ) ;
#22172=DIRECTION ( 'NONE',  ( 0.000000000000000000, 0.000000000000000000, -1.000000000000000000 ) ) ;
#22252=VECTOR ( 'NONE', #13218, 999.9999999999998863 ) ;
#22341=ORIENTED_EDGE ( 'NONE', *, *, #14300, .F. ) ;
#22351=PLANE ( 'NONE',  #13197 ) ;
#22355=DIRECTION ( 'NONE',  ( 1.000000000000000000, -8.896220237034308570E-17, 0.000000000000000000 ) ) ;
#22358=CARTESIAN_POINT ( 'NONE',  ( 31.01827548281339375, -2.500766059351008153, 15.00000000000011369 ) ) ;
#22398=UNCERTAINTY_MEASURE_WITH_UNIT (LENGTH_MEASURE( 1.000000000000000082E-05 ), #19948, 'distance_accuracy_value', 'NONE');
#22433=DIRECTION ( 'NONE',  ( 0.000000000000000000, -1.000000000000000000, 9.355573283744330345E-16 ) ) ;
#22482=CIRCLE ( 'NONE', #11136, 3.750000000000000000 ) ;
#22489=ADVANCED_FACE ( 'NONE', ( #5979 ), #22647, .T. ) ;
#22533=ORIENTED_EDGE ( 'NONE', *, *, #20669, .F. ) ;
#22561=CARTESIAN_POINT ( 'NONE',  ( 33.27705887009690144, -3.036156860537079893, 13.00000000000019895 ) ) ;
#22599=ORIENTED_EDGE ( 'NONE', *, *, #21315, .T. ) ;
#22614=ADVANCED_FACE ( 'NONE', ( #4547 ), #22351, .T. ) ;
#22630=CARTESIAN_POINT ( 'NONE',  ( 28.89837840081079889, -1.998294948772165736, 17.25000000000019895 ) ) ;
#22647=CONICAL_SURFACE ( 'NONE', #18109, 2.254620000000000513, 0.7853981633974461696 ) ;
#22758=ORIENTED_EDGE ( 'NONE', *, *, #9512, .T. ) ;
#22801=ORIENTED_EDGE ( 'NONE', *, *, #12571, .T. ) ;
#22822=EDGE_CURVE ( 'NONE', #15508, #22078, #16119, .T. ) ;
#22840=CIRCLE ( 'NONE', #451, 2.500000000000000444 ) ;
#22863=CIRCLE ( 'NONE', #3529, 2.500000000000000444 ) ;
#22864=FACE_OUTER_BOUND ( 'NONE', #23101, .T. ) ;
#22904=ORIENTED_EDGE ( 'NONE', *, *, #4585, .T. ) ;
#22915=CARTESIAN_POINT ( 'NONE',  ( 30.84445860938240003, -2.459566909556570202, 13.00000000000019895 ) ) ;
#22926=DIRECTION ( 'NONE',  ( 0.9730401042858036753, -0.2306359803922028995, -5.959266323858677443E-17 ) ) ;
#22957=LINE ( 'NONE', #4800, #8842 ) ;
#23032=EDGE_CURVE ( 'NONE', #19524, #4472, #4025, .T. ) ;
#23072=AXIS2_PLACEMENT_3D ( 'NONE', #6673, #13448, #19689 ) ;
#23101=EDGE_LOOP ( 'NONE', ( #10609, #16603, #9393, #5480 ) ) ;
#23227=ORIENTED_EDGE ( 'NONE', *, *, #14075, .F. ) ;
#23247=AXIS2_PLACEMENT_3D ( 'NONE', #19770, #10646, #18355 ) ;
#23309=PRODUCT ( '1602p_c_45', '1602p_c_45', '', ( #11216 ) ) ;
#23316=CARTESIAN_POINT ( 'NONE',  ( 31.14187293219668362, -1.979315439058051851, 11.00000000000020250 ) ) ;
#23381=DIRECTION ( 'NONE',  ( -0.2306359803922028440, -0.9730401042858034533, -4.307366329831518561E-32 ) ) ;
#23522=COLOUR_RGB('Light Blue', 0.66274510, 0.83137255, 0.94901961);
#23523=FILL_AREA_STYLE_COLOUR('',#23522);
#23524=FILL_AREA_STYLE('',(#23523));
#23525=SURFACE_STYLE_FILL_AREA(#23524);
#23526=SURFACE_SIDE_STYLE('',(#23525));
#23527=SURFACE_STYLE_USAGE(.BOTH.,#23526);
#23528=PRESENTATION_STYLE_ASSIGNMENT((#23527));
#23579=STYLED_ITEM('',(#23528),#9215);
#23580=MECHANICAL_DESIGN_GEOMETRIC_PRESENTATION_REPRESENTATION('',(#23579),#1146);
ENDSEC;
END-ISO-10303-21;
